ISO-10303-21;
HEADER;
/* Generated by software containing ST-Developer
 * from STEP Tools, Inc. (www.steptools.com) 
 */

FILE_DESCRIPTION(
/* description */ ('Torque wrench calibration arm'),
/* implementation_level */ '2;1');

FILE_NAME(
/* name */ 'Cap Screw - M6x25.step',
/* time_stamp */ '2026-10-28T03:24:52-07:00',
/* author */ (''),
/* organization */ (''),
/* preprocessor_version */ 'ST-DEVELOPER v20.2',
/* originating_system */ 'Autodesk Translation Framework v15.17.0.0',
/* authorisation */ '');

FILE_SCHEMA (('AUTOMOTIVE_DESIGN { 1 0 10303 214 3 1 1 }'));
ENDSEC;

DATA;
#10=MECHANICAL_DESIGN_GEOMETRIC_PRESENTATION_REPRESENTATION('',(#447),#12783);
#11=ORIENTED_CLOSED_SHELL('',*,#6517,.F.);
#14=BREP_WITH_VOIDS('Body1',#6516,(#11));
#331=CONICAL_SURFACE('',#7304,0.475,0.785398163397449);
#332=CONICAL_SURFACE('',#7308,0.485,0.785398163397448);
#333=CONICAL_SURFACE('',#7312,0.31,0.463647609000806);
#334=CONICAL_SURFACE('',#7316,0.27,0.785398163397448);
#364=SHAPE_REPRESENTATION_RELATIONSHIP('SRR','None',#12946,#401);
#401=ADVANCED_BREP_SHAPE_REPRESENTATION('',(#14),#12755);
#447=STYLED_ITEM('',(#13219),#14);
#592=FACE_BOUND('',#1490,.T.);
#728=PLANE('',#7302);
#729=PLANE('',#7310);
#730=PLANE('',#7318);
#731=PLANE('',#7319);
#732=PLANE('',#7320);
#733=PLANE('',#7321);
#734=PLANE('',#7322);
#735=PLANE('',#7323);
#736=PLANE('',#7324);
#737=PLANE('',#7325);
#738=PLANE('',#7326);
#1029=FACE_OUTER_BOUND('',#1485,.T.);
#1030=FACE_OUTER_BOUND('',#1486,.T.);
#1031=FACE_OUTER_BOUND('',#1487,.T.);
#1032=FACE_OUTER_BOUND('',#1488,.T.);
#1033=FACE_OUTER_BOUND('',#1489,.T.);
#1034=FACE_OUTER_BOUND('',#1491,.T.);
#1035=FACE_OUTER_BOUND('',#1492,.T.);
#1036=FACE_OUTER_BOUND('',#1493,.T.);
#1037=FACE_OUTER_BOUND('',#1494,.T.);
#1038=FACE_OUTER_BOUND('',#1495,.T.);
#1039=FACE_OUTER_BOUND('',#1496,.T.);
#1040=FACE_OUTER_BOUND('',#1497,.T.);
#1041=FACE_OUTER_BOUND('',#1498,.T.);
#1042=FACE_OUTER_BOUND('',#1499,.T.);
#1043=FACE_OUTER_BOUND('',#1500,.T.);
#1044=FACE_OUTER_BOUND('',#1501,.T.);
#1045=FACE_OUTER_BOUND('',#1502,.T.);
#1485=EDGE_LOOP('',(#5021));
#1486=EDGE_LOOP('',(#5022,#5023,#5024,#5025));
#1487=EDGE_LOOP('',(#5026,#5027,#5028,#5029));
#1488=EDGE_LOOP('',(#5030,#5031,#5032,#5033));
#1489=EDGE_LOOP('',(#5034));
#1490=EDGE_LOOP('',(#5035));
#1491=EDGE_LOOP('',(#5036,#5037,#5038,#5039));
#1492=EDGE_LOOP('',(#5040,#5041,#5042,#5043));
#1493=EDGE_LOOP('',(#5044,#5045,#5046,#5047));
#1494=EDGE_LOOP('',(#5048));
#1495=EDGE_LOOP('',(#5049,#5050,#5051,#5052));
#1496=EDGE_LOOP('',(#5053,#5054,#5055,#5056));
#1497=EDGE_LOOP('',(#5057,#5058,#5059,#5060));
#1498=EDGE_LOOP('',(#5061,#5062,#5063,#5064));
#1499=EDGE_LOOP('',(#5065,#5066,#5067,#5068));
#1500=EDGE_LOOP('',(#5069,#5070,#5071,#5072));
#1501=EDGE_LOOP('',(#5073,#5074,#5075,#5076,#5077,#5078));
#1502=EDGE_LOOP('',(#5079,#5080,#5081,#5082,#5083,#5084));
#1936=LINE('',#11053,#2351);
#1937=LINE('',#11057,#2352);
#1938=LINE('',#11061,#2353);
#1939=LINE('',#11068,#2354);
#1940=LINE('',#11072,#2355);
#1941=LINE('',#11076,#2356);
#1942=LINE('',#11081,#2357);
#1943=LINE('',#11083,#2358);
#1944=LINE('',#11085,#2359);
#1945=LINE('',#11086,#2360);
#1946=LINE('',#11089,#2361);
#1947=LINE('',#11091,#2362);
#1948=LINE('',#11092,#2363);
#1949=LINE('',#11095,#2364);
#1950=LINE('',#11097,#2365);
#1951=LINE('',#11098,#2366);
#1952=LINE('',#11101,#2367);
#1953=LINE('',#11103,#2368);
#1954=LINE('',#11104,#2369);
#1955=LINE('',#11107,#2370);
#1956=LINE('',#11109,#2371);
#1957=LINE('',#11110,#2372);
#1958=LINE('',#11112,#2373);
#1959=LINE('',#11113,#2374);
#2351=VECTOR('',#8652,0.475);
#2352=VECTOR('',#8657,0.5);
#2353=VECTOR('',#8662,0.485);
#2354=VECTOR('',#8671,0.31);
#2355=VECTOR('',#8676,0.3);
#2356=VECTOR('',#8681,0.27);
#2357=VECTOR('',#8686,1.);
#2358=VECTOR('',#8687,1.);
#2359=VECTOR('',#8688,1.);
#2360=VECTOR('',#8689,1.);
#2361=VECTOR('',#8692,1.);
#2362=VECTOR('',#8693,1.);
#2363=VECTOR('',#8694,1.);
#2364=VECTOR('',#8697,1.);
#2365=VECTOR('',#8698,1.);
#2366=VECTOR('',#8699,1.);
#2367=VECTOR('',#8702,1.);
#2368=VECTOR('',#8703,1.);
#2369=VECTOR('',#8704,1.);
#2370=VECTOR('',#8707,1.);
#2371=VECTOR('',#8708,1.);
#2372=VECTOR('',#8709,1.);
#2373=VECTOR('',#8712,1.);
#2374=VECTOR('',#8713,1.);
#2783=CIRCLE('',#7303,0.45);
#2784=CIRCLE('',#7305,0.5);
#2785=CIRCLE('',#7307,0.5);
#2786=CIRCLE('',#7309,0.47);
#2787=CIRCLE('',#7311,0.32);
#2788=CIRCLE('',#7313,0.2942);
#2789=CIRCLE('',#7315,0.2942);
#2790=CIRCLE('',#7317,0.24);
#3205=VERTEX_POINT('',#11048);
#3206=VERTEX_POINT('',#11051);
#3207=VERTEX_POINT('',#11055);
#3208=VERTEX_POINT('',#11059);
#3209=VERTEX_POINT('',#11063);
#3210=VERTEX_POINT('',#11066);
#3211=VERTEX_POINT('',#11070);
#3212=VERTEX_POINT('',#11074);
#3213=VERTEX_POINT('',#11079);
#3214=VERTEX_POINT('',#11080);
#3215=VERTEX_POINT('',#11082);
#3216=VERTEX_POINT('',#11084);
#3217=VERTEX_POINT('',#11088);
#3218=VERTEX_POINT('',#11090);
#3219=VERTEX_POINT('',#11094);
#3220=VERTEX_POINT('',#11096);
#3221=VERTEX_POINT('',#11100);
#3222=VERTEX_POINT('',#11102);
#3223=VERTEX_POINT('',#11106);
#3224=VERTEX_POINT('',#11108);
#3868=EDGE_CURVE('',#3205,#3205,#2783,.T.);
#3869=EDGE_CURVE('',#3206,#3206,#2784,.T.);
#3870=EDGE_CURVE('',#3206,#3205,#1936,.T.);
#3871=EDGE_CURVE('',#3207,#3207,#2785,.T.);
#3872=EDGE_CURVE('',#3207,#3206,#1937,.T.);
#3873=EDGE_CURVE('',#3208,#3208,#2786,.T.);
#3874=EDGE_CURVE('',#3208,#3207,#1938,.T.);
#3875=EDGE_CURVE('',#3209,#3209,#2787,.T.);
#3876=EDGE_CURVE('',#3210,#3210,#2788,.F.);
#3877=EDGE_CURVE('',#3210,#3209,#1939,.T.);
#3878=EDGE_CURVE('',#3211,#3211,#2789,.F.);
#3879=EDGE_CURVE('',#3211,#3210,#1940,.T.);
#3880=EDGE_CURVE('',#3212,#3212,#2790,.T.);
#3881=EDGE_CURVE('',#3212,#3211,#1941,.T.);
#3882=EDGE_CURVE('',#3213,#3214,#1942,.T.);
#3883=EDGE_CURVE('',#3214,#3215,#1943,.T.);
#3884=EDGE_CURVE('',#3215,#3216,#1944,.T.);
#3885=EDGE_CURVE('',#3213,#3216,#1945,.T.);
#3886=EDGE_CURVE('',#3214,#3217,#1946,.T.);
#3887=EDGE_CURVE('',#3217,#3218,#1947,.T.);
#3888=EDGE_CURVE('',#3218,#3215,#1948,.T.);
#3889=EDGE_CURVE('',#3217,#3219,#1949,.T.);
#3890=EDGE_CURVE('',#3219,#3220,#1950,.T.);
#3891=EDGE_CURVE('',#3220,#3218,#1951,.T.);
#3892=EDGE_CURVE('',#3219,#3221,#1952,.T.);
#3893=EDGE_CURVE('',#3221,#3222,#1953,.T.);
#3894=EDGE_CURVE('',#3222,#3220,#1954,.T.);
#3895=EDGE_CURVE('',#3221,#3223,#1955,.T.);
#3896=EDGE_CURVE('',#3223,#3224,#1956,.T.);
#3897=EDGE_CURVE('',#3224,#3222,#1957,.T.);
#3898=EDGE_CURVE('',#3223,#3213,#1958,.T.);
#3899=EDGE_CURVE('',#3216,#3224,#1959,.T.);
#5021=ORIENTED_EDGE('',*,*,#3868,.F.);
#5022=ORIENTED_EDGE('',*,*,#3869,.F.);
#5023=ORIENTED_EDGE('',*,*,#3870,.T.);
#5024=ORIENTED_EDGE('',*,*,#3868,.T.);
#5025=ORIENTED_EDGE('',*,*,#3870,.F.);
#5026=ORIENTED_EDGE('',*,*,#3871,.F.);
#5027=ORIENTED_EDGE('',*,*,#3872,.T.);
#5028=ORIENTED_EDGE('',*,*,#3869,.T.);
#5029=ORIENTED_EDGE('',*,*,#3872,.F.);
#5030=ORIENTED_EDGE('',*,*,#3873,.F.);
#5031=ORIENTED_EDGE('',*,*,#3874,.T.);
#5032=ORIENTED_EDGE('',*,*,#3871,.T.);
#5033=ORIENTED_EDGE('',*,*,#3874,.F.);
#5034=ORIENTED_EDGE('',*,*,#3873,.T.);
#5035=ORIENTED_EDGE('',*,*,#3875,.F.);
#5036=ORIENTED_EDGE('',*,*,#3876,.F.);
#5037=ORIENTED_EDGE('',*,*,#3877,.T.);
#5038=ORIENTED_EDGE('',*,*,#3875,.T.);
#5039=ORIENTED_EDGE('',*,*,#3877,.F.);
#5040=ORIENTED_EDGE('',*,*,#3878,.F.);
#5041=ORIENTED_EDGE('',*,*,#3879,.T.);
#5042=ORIENTED_EDGE('',*,*,#3876,.T.);
#5043=ORIENTED_EDGE('',*,*,#3879,.F.);
#5044=ORIENTED_EDGE('',*,*,#3880,.F.);
#5045=ORIENTED_EDGE('',*,*,#3881,.T.);
#5046=ORIENTED_EDGE('',*,*,#3878,.T.);
#5047=ORIENTED_EDGE('',*,*,#3881,.F.);
#5048=ORIENTED_EDGE('',*,*,#3880,.T.);
#5049=ORIENTED_EDGE('',*,*,#3882,.T.);
#5050=ORIENTED_EDGE('',*,*,#3883,.T.);
#5051=ORIENTED_EDGE('',*,*,#3884,.T.);
#5052=ORIENTED_EDGE('',*,*,#3885,.F.);
#5053=ORIENTED_EDGE('',*,*,#3886,.T.);
#5054=ORIENTED_EDGE('',*,*,#3887,.T.);
#5055=ORIENTED_EDGE('',*,*,#3888,.T.);
#5056=ORIENTED_EDGE('',*,*,#3883,.F.);
#5057=ORIENTED_EDGE('',*,*,#3889,.T.);
#5058=ORIENTED_EDGE('',*,*,#3890,.T.);
#5059=ORIENTED_EDGE('',*,*,#3891,.T.);
#5060=ORIENTED_EDGE('',*,*,#3887,.F.);
#5061=ORIENTED_EDGE('',*,*,#3892,.T.);
#5062=ORIENTED_EDGE('',*,*,#3893,.T.);
#5063=ORIENTED_EDGE('',*,*,#3894,.T.);
#5064=ORIENTED_EDGE('',*,*,#3890,.F.);
#5065=ORIENTED_EDGE('',*,*,#3895,.T.);
#5066=ORIENTED_EDGE('',*,*,#3896,.T.);
#5067=ORIENTED_EDGE('',*,*,#3897,.T.);
#5068=ORIENTED_EDGE('',*,*,#3893,.F.);
#5069=ORIENTED_EDGE('',*,*,#3898,.T.);
#5070=ORIENTED_EDGE('',*,*,#3885,.T.);
#5071=ORIENTED_EDGE('',*,*,#3899,.T.);
#5072=ORIENTED_EDGE('',*,*,#3896,.F.);
#5073=ORIENTED_EDGE('',*,*,#3898,.F.);
#5074=ORIENTED_EDGE('',*,*,#3895,.F.);
#5075=ORIENTED_EDGE('',*,*,#3892,.F.);
#5076=ORIENTED_EDGE('',*,*,#3889,.F.);
#5077=ORIENTED_EDGE('',*,*,#3886,.F.);
#5078=ORIENTED_EDGE('',*,*,#3882,.F.);
#5079=ORIENTED_EDGE('',*,*,#3899,.F.);
#5080=ORIENTED_EDGE('',*,*,#3884,.F.);
#5081=ORIENTED_EDGE('',*,*,#3888,.F.);
#5082=ORIENTED_EDGE('',*,*,#3891,.F.);
#5083=ORIENTED_EDGE('',*,*,#3894,.F.);
#5084=ORIENTED_EDGE('',*,*,#3897,.F.);
#6041=CYLINDRICAL_SURFACE('',#7306,0.5);
#6042=CYLINDRICAL_SURFACE('',#7314,0.2942);
#6254=ADVANCED_FACE('',(#1029),#728,.T.);
#6255=ADVANCED_FACE('',(#1030),#331,.T.);
#6256=ADVANCED_FACE('',(#1031),#6041,.T.);
#6257=ADVANCED_FACE('',(#1032),#332,.T.);
#6258=ADVANCED_FACE('',(#1033,#592),#729,.T.);
#6259=ADVANCED_FACE('',(#1034),#333,.T.);
#6260=ADVANCED_FACE('',(#1035),#6042,.T.);
#6261=ADVANCED_FACE('',(#1036),#334,.T.);
#6262=ADVANCED_FACE('',(#1037),#730,.T.);
#6263=ADVANCED_FACE('',(#1038),#731,.F.);
#6264=ADVANCED_FACE('',(#1039),#732,.F.);
#6265=ADVANCED_FACE('',(#1040),#733,.F.);
#6266=ADVANCED_FACE('',(#1041),#734,.F.);
#6267=ADVANCED_FACE('',(#1042),#735,.F.);
#6268=ADVANCED_FACE('',(#1043),#736,.F.);
#6269=ADVANCED_FACE('',(#1044),#737,.F.);
#6270=ADVANCED_FACE('',(#1045),#738,.F.);
#6516=CLOSED_SHELL('',(#6254,#6255,#6256,#6257,#6258,#6259,#6260,#6261,
#6262));
#6517=CLOSED_SHELL('',(#6263,#6264,#6265,#6266,#6267,#6268,#6269,#6270));
#7301=AXIS2_PLACEMENT_3D('',#11046,#8642,#8643);
#7302=AXIS2_PLACEMENT_3D('',#11047,#8644,#8645);
#7303=AXIS2_PLACEMENT_3D('',#11049,#8646,#8647);
#7304=AXIS2_PLACEMENT_3D('',#11050,#8648,#8649);
#7305=AXIS2_PLACEMENT_3D('',#11052,#8650,#8651);
#7306=AXIS2_PLACEMENT_3D('',#11054,#8653,#8654);
#7307=AXIS2_PLACEMENT_3D('',#11056,#8655,#8656);
#7308=AXIS2_PLACEMENT_3D('',#11058,#8658,#8659);
#7309=AXIS2_PLACEMENT_3D('',#11060,#8660,#8661);
#7310=AXIS2_PLACEMENT_3D('',#11062,#8663,#8664);
#7311=AXIS2_PLACEMENT_3D('',#11064,#8665,#8666);
#7312=AXIS2_PLACEMENT_3D('',#11065,#8667,#8668);
#7313=AXIS2_PLACEMENT_3D('',#11067,#8669,#8670);
#7314=AXIS2_PLACEMENT_3D('',#11069,#8672,#8673);
#7315=AXIS2_PLACEMENT_3D('',#11071,#8674,#8675);
#7316=AXIS2_PLACEMENT_3D('',#11073,#8677,#8678);
#7317=AXIS2_PLACEMENT_3D('',#11075,#8679,#8680);
#7318=AXIS2_PLACEMENT_3D('',#11077,#8682,#8683);
#7319=AXIS2_PLACEMENT_3D('',#11078,#8684,#8685);
#7320=AXIS2_PLACEMENT_3D('',#11087,#8690,#8691);
#7321=AXIS2_PLACEMENT_3D('',#11093,#8695,#8696);
#7322=AXIS2_PLACEMENT_3D('',#11099,#8700,#8701);
#7323=AXIS2_PLACEMENT_3D('',#11105,#8705,#8706);
#7324=AXIS2_PLACEMENT_3D('',#11111,#8710,#8711);
#7325=AXIS2_PLACEMENT_3D('',#11114,#8714,#8715);
#7326=AXIS2_PLACEMENT_3D('',#11115,#8716,#8717);
#8642=DIRECTION('axis',(0.,0.,1.));
#8643=DIRECTION('refdir',(1.,0.,0.));
#8644=DIRECTION('center_axis',(0.,1.,0.));
#8645=DIRECTION('ref_axis',(0.,0.,1.));
#8646=DIRECTION('center_axis',(0.,-1.,0.));
#8647=DIRECTION('ref_axis',(1.,0.,0.));
#8648=DIRECTION('center_axis',(0.,-1.,0.));
#8649=DIRECTION('ref_axis',(1.,0.,0.));
#8650=DIRECTION('center_axis',(0.,-1.,0.));
#8651=DIRECTION('ref_axis',(1.,0.,0.));
#8652=DIRECTION('',(0.707106781186548,0.707106781186547,8.65956056235494E-17));
#8653=DIRECTION('center_axis',(0.,-1.,0.));
#8654=DIRECTION('ref_axis',(1.,0.,0.));
#8655=DIRECTION('center_axis',(0.,-1.,0.));
#8656=DIRECTION('ref_axis',(1.,0.,0.));
#8657=DIRECTION('',(0.,1.,0.));
#8658=DIRECTION('center_axis',(0.,1.,0.));
#8659=DIRECTION('ref_axis',(1.,0.,0.));
#8660=DIRECTION('center_axis',(0.,-1.,0.));
#8661=DIRECTION('ref_axis',(1.,0.,0.));
#8662=DIRECTION('',(-0.707106781186547,0.707106781186548,-8.65956056235493E-17));
#8663=DIRECTION('center_axis',(0.,-1.,0.));
#8664=DIRECTION('ref_axis',(0.,0.,-1.));
#8665=DIRECTION('center_axis',(0.,-1.,0.));
#8666=DIRECTION('ref_axis',(1.,0.,0.));
#8667=DIRECTION('center_axis',(0.,1.,0.));
#8668=DIRECTION('ref_axis',(1.,0.,0.));
#8669=DIRECTION('center_axis',(0.,1.,0.));
#8670=DIRECTION('ref_axis',(1.,0.,0.));
#8671=DIRECTION('',(-0.447213595499958,0.894427190999916,-5.47678698264203E-17));
#8672=DIRECTION('center_axis',(0.,-1.,0.));
#8673=DIRECTION('ref_axis',(1.,0.,0.));
#8674=DIRECTION('center_axis',(0.,1.,0.));
#8675=DIRECTION('ref_axis',(1.,0.,0.));
#8676=DIRECTION('',(0.,1.,0.));
#8677=DIRECTION('center_axis',(0.,1.,0.));
#8678=DIRECTION('ref_axis',(1.,0.,0.));
#8679=DIRECTION('center_axis',(0.,-1.,0.));
#8680=DIRECTION('ref_axis',(1.,0.,0.));
#8681=DIRECTION('',(-0.707106781186547,0.707106781186548,-8.65956056235493E-17));
#8682=DIRECTION('center_axis',(0.,-1.,0.));
#8683=DIRECTION('ref_axis',(0.,0.,-1.));
#8684=DIRECTION('center_axis',(0.866025403784439,0.,-0.5));
#8685=DIRECTION('ref_axis',(0.5,0.,0.866025403784439));
#8686=DIRECTION('',(-0.5,0.,-0.866025403784439));
#8687=DIRECTION('',(0.,-1.,0.));
#8688=DIRECTION('',(0.5,0.,0.866025403784439));
#8689=DIRECTION('',(0.,-1.,0.));
#8690=DIRECTION('center_axis',(1.92296268638356E-16,0.,-1.));
#8691=DIRECTION('ref_axis',(1.,0.,1.92296268638356E-16));
#8692=DIRECTION('',(-1.,0.,-1.92296268638356E-16));
#8693=DIRECTION('',(0.,-1.,0.));
#8694=DIRECTION('',(1.,0.,1.92296268638356E-16));
#8695=DIRECTION('center_axis',(-0.866025403784439,0.,-0.5));
#8696=DIRECTION('ref_axis',(0.5,0.,-0.866025403784439));
#8697=DIRECTION('',(-0.5,0.,0.866025403784438));
#8698=DIRECTION('',(0.,-1.,0.));
#8699=DIRECTION('',(0.5,0.,-0.866025403784438));
#8700=DIRECTION('center_axis',(-0.866025403784439,0.,0.5));
#8701=DIRECTION('ref_axis',(-0.5,0.,-0.866025403784439));
#8702=DIRECTION('',(0.5,0.,0.866025403784439));
#8703=DIRECTION('',(0.,-1.,0.));
#8704=DIRECTION('',(-0.5,0.,-0.866025403784439));
#8705=DIRECTION('center_axis',(-1.92296268638356E-16,0.,1.));
#8706=DIRECTION('ref_axis',(-1.,0.,-1.92296268638356E-16));
#8707=DIRECTION('',(1.,0.,1.92296268638356E-16));
#8708=DIRECTION('',(0.,-1.,0.));
#8709=DIRECTION('',(-1.,0.,-1.92296268638356E-16));
#8710=DIRECTION('center_axis',(0.866025403784439,0.,0.5));
#8711=DIRECTION('ref_axis',(-0.5,0.,0.866025403784439));
#8712=DIRECTION('',(0.5,0.,-0.866025403784439));
#8713=DIRECTION('',(-0.5,0.,0.866025403784439));
#8714=DIRECTION('center_axis',(0.,1.,0.));
#8715=DIRECTION('ref_axis',(1.,0.,0.));
#8716=DIRECTION('center_axis',(0.,-1.,0.));
#8717=DIRECTION('ref_axis',(0.,0.,-1.));
#11046=CARTESIAN_POINT('',(0.,0.,0.));
#11047=CARTESIAN_POINT('Origin',(0.45,0.6,0.));
#11048=CARTESIAN_POINT('',(-0.45,0.6,-5.51091059616309E-17));
#11049=CARTESIAN_POINT('Origin',(0.,0.6,0.));
#11050=CARTESIAN_POINT('Origin',(0.,0.575,0.));
#11051=CARTESIAN_POINT('',(-0.5,0.55,-6.12323399573677E-17));
#11052=CARTESIAN_POINT('Origin',(0.,0.55,0.));
#11053=CARTESIAN_POINT('',(-0.475,0.575,-5.81707229594993E-17));
#11054=CARTESIAN_POINT('Origin',(0.,0.29,0.));
#11055=CARTESIAN_POINT('',(-0.5,0.0299999999999998,-6.12323399573677E-17));
#11056=CARTESIAN_POINT('Origin',(0.,0.0299999999999998,0.));
#11057=CARTESIAN_POINT('',(-0.5,0.29,-6.12323399573677E-17));
#11058=CARTESIAN_POINT('Origin',(0.,0.0150000000000001,0.));
#11059=CARTESIAN_POINT('',(-0.47,7.11236625150491E-17,-5.75583995599256E-17));
#11060=CARTESIAN_POINT('Origin',(0.,0.,0.));
#11061=CARTESIAN_POINT('',(-0.485,0.0150000000000001,-5.93953697586466E-17));
#11062=CARTESIAN_POINT('Origin',(0.32,0.,0.));
#11063=CARTESIAN_POINT('',(-0.32,-6.93889390390723E-18,-3.91886975727153E-17));
#11064=CARTESIAN_POINT('Origin',(0.,0.,0.));
#11065=CARTESIAN_POINT('Origin',(0.,-0.02,0.));
#11066=CARTESIAN_POINT('',(-0.2942,-0.0515999999999999,3.60291088309151E-17));
#11067=CARTESIAN_POINT('Origin',(0.,-0.0515999999999999,0.));
#11068=CARTESIAN_POINT('',(-0.31,-0.02,-3.7964050773568E-17));
#11069=CARTESIAN_POINT('Origin',(0.,-1.24,0.));
#11070=CARTESIAN_POINT('',(-0.2942,-2.4458,3.60291088309151E-17));
#11071=CARTESIAN_POINT('Origin',(0.,-2.4458,0.));
#11072=CARTESIAN_POINT('',(-0.2942,-1.24,-3.60291088309151E-17));
#11073=CARTESIAN_POINT('Origin',(0.,-2.47,0.));
#11074=CARTESIAN_POINT('',(-0.24,-2.5,-2.93915231795365E-17));
#11075=CARTESIAN_POINT('Origin',(0.,-2.5,0.));
#11076=CARTESIAN_POINT('',(-0.27,-2.47,-3.30654635769785E-17));
#11077=CARTESIAN_POINT('Origin',(0.,-2.5,0.));
#11078=CARTESIAN_POINT('Origin',(0.144337567297406,-0.6,-0.25));
#11079=CARTESIAN_POINT('',(0.288675134594813,-0.6,0.));
#11080=CARTESIAN_POINT('',(0.144337567297406,-0.6,-0.25));
#11081=CARTESIAN_POINT('',(0.288675134594813,-0.6,0.));
#11082=CARTESIAN_POINT('',(0.144337567297406,-0.96,-0.25));
#11083=CARTESIAN_POINT('',(0.144337567297406,-0.6,-0.25));
#11084=CARTESIAN_POINT('',(0.288675134594813,-0.96,0.));
#11085=CARTESIAN_POINT('',(0.288675134594813,-0.96,0.));
#11086=CARTESIAN_POINT('',(0.288675134594813,-0.6,0.));
#11087=CARTESIAN_POINT('Origin',(-0.144337567297406,-0.6,-0.25));
#11088=CARTESIAN_POINT('',(-0.144337567297406,-0.6,-0.25));
#11089=CARTESIAN_POINT('',(0.144337567297406,-0.6,-0.25));
#11090=CARTESIAN_POINT('',(-0.144337567297406,-0.96,-0.25));
#11091=CARTESIAN_POINT('',(-0.144337567297406,-0.6,-0.25));
#11092=CARTESIAN_POINT('',(0.144337567297406,-0.96,-0.25));
#11093=CARTESIAN_POINT('Origin',(-0.288675134594813,-0.6,-8.32667268468867E-17));
#11094=CARTESIAN_POINT('',(-0.288675134594813,-0.6,-3.53525079574969E-17));
#11095=CARTESIAN_POINT('',(-0.144337567297406,-0.6,-0.25));
#11096=CARTESIAN_POINT('',(-0.288675134594813,-0.96,-5.55111512312578E-17));
#11097=CARTESIAN_POINT('',(-0.288675134594813,-0.6,-3.53525079574969E-17));
#11098=CARTESIAN_POINT('',(-0.144337567297406,-0.96,-0.25));
#11099=CARTESIAN_POINT('Origin',(-0.144337567297407,-0.6,0.25));
#11100=CARTESIAN_POINT('',(-0.144337567297407,-0.6,0.25));
#11101=CARTESIAN_POINT('',(-0.288675134594813,-0.6,-3.53525079574969E-17));
#11102=CARTESIAN_POINT('',(-0.144337567297407,-0.96,0.25));
#11103=CARTESIAN_POINT('',(-0.144337567297407,-0.6,0.25));
#11104=CARTESIAN_POINT('',(-0.288675134594813,-0.96,-3.53525079574969E-17));
#11105=CARTESIAN_POINT('Origin',(0.144337567297406,-0.6,0.25));
#11106=CARTESIAN_POINT('',(0.144337567297406,-0.6,0.25));
#11107=CARTESIAN_POINT('',(-0.144337567297407,-0.6,0.25));
#11108=CARTESIAN_POINT('',(0.144337567297406,-0.96,0.25));
#11109=CARTESIAN_POINT('',(0.144337567297406,-0.6,0.25));
#11110=CARTESIAN_POINT('',(-0.144337567297407,-0.96,0.25));
#11111=CARTESIAN_POINT('Origin',(0.288675134594813,-0.6,0.));
#11112=CARTESIAN_POINT('',(0.144337567297406,-0.6,0.25));
#11113=CARTESIAN_POINT('',(0.144337567297406,-0.96,0.25));
#11114=CARTESIAN_POINT('Origin',(0.,-0.6,0.));
#11115=CARTESIAN_POINT('Origin',(0.,-0.96,0.));
#12711=UNCERTAINTY_MEASURE_WITH_UNIT(LENGTH_MEASURE(0.001),#12784,
'DISTANCE_ACCURACY_VALUE',
'Maximum model space distance between geometric entities at asserted c
onnectivities');
#12739=UNCERTAINTY_MEASURE_WITH_UNIT(LENGTH_MEASURE(0.001),#12784,
'DISTANCE_ACCURACY_VALUE',
'Maximum model space distance between geometric entities at asserted c
onnectivities');
#12755=(
GEOMETRIC_REPRESENTATION_CONTEXT(3)
GLOBAL_UNCERTAINTY_ASSIGNED_CONTEXT((#12711))
GLOBAL_UNIT_ASSIGNED_CONTEXT((#12784,#12786,#12787))
REPRESENTATION_CONTEXT('','3D')
);
#12783=(
GEOMETRIC_REPRESENTATION_CONTEXT(3)
GLOBAL_UNCERTAINTY_ASSIGNED_CONTEXT((#12739))
GLOBAL_UNIT_ASSIGNED_CONTEXT((#12784,#12786,#12787))
REPRESENTATION_CONTEXT('','3D')
);
#12784=(
LENGTH_UNIT()
NAMED_UNIT(*)
SI_UNIT(.CENTI.,.METRE.)
);
#12786=(
NAMED_UNIT(*)
PLANE_ANGLE_UNIT()
SI_UNIT($,.RADIAN.)
);
#12787=(
NAMED_UNIT(*)
SI_UNIT($,.STERADIAN.)
SOLID_ANGLE_UNIT()
);
#12803=SHAPE_DEFINITION_REPRESENTATION(#12851,#12946);
#12851=PRODUCT_DEFINITION_SHAPE('',$,#12990);
#12946=SHAPE_REPRESENTATION('',(#7301),#12755);
#12974=PRODUCT_DEFINITION_CONTEXT('part definition',#13105,'design');
#12990=PRODUCT_DEFINITION('Cap Screw - M6x25','Cap Screw - M6x25',#13033,
#12974);
#13033=PRODUCT_DEFINITION_FORMATION('',$,#13122);
#13105=APPLICATION_CONTEXT(
'Core Data for Automotive Mechanical Design Process');
#13106=PRODUCT_CONTEXT('part definition',#13105,'mechanical');
#13122=PRODUCT('Cap Screw - M6x25','Cap Screw - M6x25',
'Cap Screw - M6x25',(#13106));
#13213=COLOUR_RGB('Black',0.12,0.14,0.17);
#13214=FILL_AREA_STYLE_COLOUR('',#13213);
#13215=FILL_AREA_STYLE('',(#13214));
#13216=SURFACE_STYLE_FILL_AREA(#13215);
#13217=SURFACE_SIDE_STYLE('',(#13216));
#13218=SURFACE_STYLE_USAGE(.BOTH.,#13217);
#13219=PRESENTATION_STYLE_ASSIGNMENT((#13218));
ENDSEC;
END-ISO-10303-21;
